ISO-10303-21;
HEADER;
/* Generated by software containing ST-Developer
 * from STEP Tools, Inc. (www.steptools.com) 
 */

FILE_DESCRIPTION(
/* description */ ('Bell-crank linkage with push rods'),
/* implementation_level */ '2;1');

FILE_NAME(
/* name */ 'Upper pin sleeve (1).step',
/* time_stamp */ '2026-10-28T03:25:15-07:00',
/* author */ (''),
/* organization */ (''),
/* preprocessor_version */ 'ST-DEVELOPER v20.2',
/* originating_system */ 'Autodesk Translation Framework v15.17.0.0',
/* authorisation */ '');

FILE_SCHEMA (('AUTOMOTIVE_DESIGN { 1 0 10303 214 3 1 1 }'));
ENDSEC;

DATA;
#10=MECHANICAL_DESIGN_GEOMETRIC_PRESENTATION_REPRESENTATION('',(#639),#16678);
#523=SHAPE_REPRESENTATION_RELATIONSHIP('SRR','None',#16941,#577);
#577=ADVANCED_BREP_SHAPE_REPRESENTATION('',(#700),#16646);
#639=STYLED_ITEM('',(#17291),#700);
#700=MANIFOLD_SOLID_BREP('Body1',#8830);
#852=FACE_BOUND('',#2200,.T.);
#853=FACE_BOUND('',#2202,.T.);
#1119=PLANE('',#10104);
#1120=PLANE('',#10105);
#1548=FACE_OUTER_BOUND('',#2197,.T.);
#1549=FACE_OUTER_BOUND('',#2198,.T.);
#1550=FACE_OUTER_BOUND('',#2199,.T.);
#1551=FACE_OUTER_BOUND('',#2201,.T.);
#2197=EDGE_LOOP('',(#7201,#7202,#7203,#7204));
#2198=EDGE_LOOP('',(#7205,#7206,#7207,#7208));
#2199=EDGE_LOOP('',(#7209));
#2200=EDGE_LOOP('',(#7210));
#2201=EDGE_LOOP('',(#7211));
#2202=EDGE_LOOP('',(#7212));
#2832=LINE('',#15488,#3381);
#2833=LINE('',#15494,#3382);
#3381=VECTOR('',#12222,0.305);
#3382=VECTOR('',#12229,0.5);
#3936=CIRCLE('',#10099,0.305);
#3937=CIRCLE('',#10100,0.305);
#3938=CIRCLE('',#10102,0.5);
#3939=CIRCLE('',#10103,0.5);
#4547=VERTEX_POINT('',#15485);
#4548=VERTEX_POINT('',#15487);
#4549=VERTEX_POINT('',#15491);
#4550=VERTEX_POINT('',#15493);
#5478=EDGE_CURVE('',#4547,#4547,#3936,.T.);
#5479=EDGE_CURVE('',#4547,#4548,#2832,.T.);
#5480=EDGE_CURVE('',#4548,#4548,#3937,.T.);
#5481=EDGE_CURVE('',#4549,#4549,#3938,.T.);
#5482=EDGE_CURVE('',#4549,#4550,#2833,.T.);
#5483=EDGE_CURVE('',#4550,#4550,#3939,.T.);
#7201=ORIENTED_EDGE('',*,*,#5478,.F.);
#7202=ORIENTED_EDGE('',*,*,#5479,.T.);
#7203=ORIENTED_EDGE('',*,*,#5480,.T.);
#7204=ORIENTED_EDGE('',*,*,#5479,.F.);
#7205=ORIENTED_EDGE('',*,*,#5481,.F.);
#7206=ORIENTED_EDGE('',*,*,#5482,.T.);
#7207=ORIENTED_EDGE('',*,*,#5483,.T.);
#7208=ORIENTED_EDGE('',*,*,#5482,.F.);
#7209=ORIENTED_EDGE('',*,*,#5481,.T.);
#7210=ORIENTED_EDGE('',*,*,#5478,.T.);
#7211=ORIENTED_EDGE('',*,*,#5483,.F.);
#7212=ORIENTED_EDGE('',*,*,#5480,.F.);
#8187=CYLINDRICAL_SURFACE('',#10098,0.305);
#8188=CYLINDRICAL_SURFACE('',#10101,0.5);
#8573=ADVANCED_FACE('',(#1548),#8187,.F.);
#8574=ADVANCED_FACE('',(#1549),#8188,.T.);
#8575=ADVANCED_FACE('',(#1550,#852),#1119,.T.);
#8576=ADVANCED_FACE('',(#1551,#853),#1120,.F.);
#8830=CLOSED_SHELL('',(#8573,#8574,#8575,#8576));
#10097=AXIS2_PLACEMENT_3D('',#15483,#12216,#12217);
#10098=AXIS2_PLACEMENT_3D('',#15484,#12218,#12219);
#10099=AXIS2_PLACEMENT_3D('',#15486,#12220,#12221);
#10100=AXIS2_PLACEMENT_3D('',#15489,#12223,#12224);
#10101=AXIS2_PLACEMENT_3D('',#15490,#12225,#12226);
#10102=AXIS2_PLACEMENT_3D('',#15492,#12227,#12228);
#10103=AXIS2_PLACEMENT_3D('',#15495,#12230,#12231);
#10104=AXIS2_PLACEMENT_3D('',#15496,#12232,#12233);
#10105=AXIS2_PLACEMENT_3D('',#15497,#12234,#12235);
#12216=DIRECTION('axis',(0.,0.,1.));
#12217=DIRECTION('refdir',(1.,0.,0.));
#12218=DIRECTION('center_axis',(0.,0.,1.));
#12219=DIRECTION('ref_axis',(1.,0.,0.));
#12220=DIRECTION('center_axis',(0.,0.,-1.));
#12221=DIRECTION('ref_axis',(1.,0.,0.));
#12222=DIRECTION('',(0.,0.,-1.));
#12223=DIRECTION('center_axis',(0.,0.,-1.));
#12224=DIRECTION('ref_axis',(1.,0.,0.));
#12225=DIRECTION('center_axis',(0.,0.,1.));
#12226=DIRECTION('ref_axis',(1.,0.,0.));
#12227=DIRECTION('center_axis',(0.,0.,1.));
#12228=DIRECTION('ref_axis',(1.,0.,0.));
#12229=DIRECTION('',(0.,0.,-1.));
#12230=DIRECTION('center_axis',(0.,0.,1.));
#12231=DIRECTION('ref_axis',(1.,0.,0.));
#12232=DIRECTION('center_axis',(0.,0.,1.));
#12233=DIRECTION('ref_axis',(1.,0.,0.));
#12234=DIRECTION('center_axis',(0.,0.,1.));
#12235=DIRECTION('ref_axis',(1.,0.,0.));
#15483=CARTESIAN_POINT('',(0.,0.,0.));
#15484=CARTESIAN_POINT('Origin',(4.,0.,7.6));
#15485=CARTESIAN_POINT('',(3.695,-3.73517273739942E-17,8.1));
#15486=CARTESIAN_POINT('Origin',(4.,0.,8.1));
#15487=CARTESIAN_POINT('',(3.695,-3.73517273739942E-17,7.6));
#15488=CARTESIAN_POINT('',(3.695,-3.73517273739942E-17,7.6));
#15489=CARTESIAN_POINT('Origin',(4.,0.,7.6));
#15490=CARTESIAN_POINT('Origin',(4.,0.,7.6));
#15491=CARTESIAN_POINT('',(3.5,-6.12323399573677E-17,8.1));
#15492=CARTESIAN_POINT('Origin',(4.,0.,8.1));
#15493=CARTESIAN_POINT('',(3.5,-6.12323399573677E-17,7.6));
#15494=CARTESIAN_POINT('',(3.5,-6.12323399573677E-17,7.6));
#15495=CARTESIAN_POINT('Origin',(4.,0.,7.6));
#15496=CARTESIAN_POINT('Origin',(4.,0.,8.1));
#15497=CARTESIAN_POINT('Origin',(4.,0.,7.6));
#16582=UNCERTAINTY_MEASURE_WITH_UNIT(LENGTH_MEASURE(0.001),#16679,
'DISTANCE_ACCURACY_VALUE',
'Maximum model space distance between geometric entities at asserted c
onnectivities');
#16614=UNCERTAINTY_MEASURE_WITH_UNIT(LENGTH_MEASURE(0.001),#16679,
'DISTANCE_ACCURACY_VALUE',
'Maximum model space distance between geometric entities at asserted c
onnectivities');
#16646=(
GEOMETRIC_REPRESENTATION_CONTEXT(3)
GLOBAL_UNCERTAINTY_ASSIGNED_CONTEXT((#16582))
GLOBAL_UNIT_ASSIGNED_CONTEXT((#16679,#16681,#16682))
REPRESENTATION_CONTEXT('','3D')
);
#16678=(
GEOMETRIC_REPRESENTATION_CONTEXT(3)
GLOBAL_UNCERTAINTY_ASSIGNED_CONTEXT((#16614))
GLOBAL_UNIT_ASSIGNED_CONTEXT((#16679,#16681,#16682))
REPRESENTATION_CONTEXT('','3D')
);
#16679=(
LENGTH_UNIT()
NAMED_UNIT(*)
SI_UNIT(.CENTI.,.METRE.)
);
#16681=(
NAMED_UNIT(*)
PLANE_ANGLE_UNIT()
SI_UNIT($,.RADIAN.)
);
#16682=(
NAMED_UNIT(*)
SI_UNIT($,.STERADIAN.)
SOLID_ANGLE_UNIT()
);
#16714=SHAPE_DEFINITION_REPRESENTATION(#16782,#16941);
#16782=PRODUCT_DEFINITION_SHAPE('',$,#17005);
#16941=SHAPE_REPRESENTATION('',(#10097),#16646);
#16973=PRODUCT_DEFINITION_CONTEXT('part definition',#17164,'design');
#17005=PRODUCT_DEFINITION('Upper pin sleeve (1)','Upper pin sleeve (1)',#17068,
#16973);
#17068=PRODUCT_DEFINITION_FORMATION('',$,#17197);
#17164=APPLICATION_CONTEXT(
'Core Data for Automotive Mechanical Design Process');
#17165=PRODUCT_CONTEXT('part definition',#17164,'mechanical');
#17197=PRODUCT('Upper pin sleeve (1)','Upper pin sleeve (1)',
'Upper pin sleeve (1)',(#17165));
#17285=COLOUR_RGB('Grey',0.48,0.52,0.57);
#17286=FILL_AREA_STYLE_COLOUR('',#17285);
#17287=FILL_AREA_STYLE('',(#17286));
#17288=SURFACE_STYLE_FILL_AREA(#17287);
#17289=SURFACE_SIDE_STYLE('',(#17288));
#17290=SURFACE_STYLE_USAGE(.BOTH.,#17289);
#17291=PRESENTATION_STYLE_ASSIGNMENT((#17290));
ENDSEC;
END-ISO-10303-21;
